ISO-10303-21;
HEADER;
/* Generated by software containing ST-Developer
 * from STEP Tools, Inc. (www.steptools.com) 
 */

FILE_DESCRIPTION(
/* description */ ('Indexing fixture plate with plunger'),
/* implementation_level */ '2;1');

FILE_NAME(
/* name */ 'Flat Washer - M6.step',
/* time_stamp */ '2026-10-28T03:23:41-07:00',
/* author */ (''),
/* organization */ (''),
/* preprocessor_version */ 'ST-DEVELOPER v20.2',
/* originating_system */ 'Autodesk Translation Framework v15.17.0.0',
/* authorisation */ '');

FILE_SCHEMA (('AUTOMOTIVE_DESIGN { 1 0 10303 214 3 1 1 }'));
ENDSEC;

DATA;
#10=MECHANICAL_DESIGN_GEOMETRIC_PRESENTATION_REPRESENTATION('',(#328),#10020);
#274=SHAPE_REPRESENTATION_RELATIONSHIP('SRR','None',#10148,#301);
#301=ADVANCED_BREP_SHAPE_REPRESENTATION('',(#364),#10001);
#328=STYLED_ITEM('',(#10375),#364);
#364=MANIFOLD_SOLID_BREP('Body1',#4582);
#428=FACE_BOUND('',#1066,.T.);
#429=FACE_BOUND('',#1068,.T.);
#570=PLANE('',#5058);
#571=PLANE('',#5059);
#736=FACE_OUTER_BOUND('',#1063,.T.);
#737=FACE_OUTER_BOUND('',#1064,.T.);
#738=FACE_OUTER_BOUND('',#1065,.T.);
#739=FACE_OUTER_BOUND('',#1067,.T.);
#1063=EDGE_LOOP('',(#3299,#3300,#3301,#3302));
#1064=EDGE_LOOP('',(#3303,#3304,#3305,#3306));
#1065=EDGE_LOOP('',(#3307));
#1066=EDGE_LOOP('',(#3308));
#1067=EDGE_LOOP('',(#3309));
#1068=EDGE_LOOP('',(#3310));
#1438=LINE('',#8521,#1658);
#1439=LINE('',#8527,#1659);
#1658=VECTOR('',#5913,0.32);
#1659=VECTOR('',#5920,0.6);
#1898=CIRCLE('',#5053,0.32);
#1899=CIRCLE('',#5054,0.32);
#1900=CIRCLE('',#5056,0.6);
#1901=CIRCLE('',#5057,0.6);
#2214=VERTEX_POINT('',#8518);
#2215=VERTEX_POINT('',#8520);
#2216=VERTEX_POINT('',#8524);
#2217=VERTEX_POINT('',#8526);
#2629=EDGE_CURVE('',#2214,#2214,#1898,.T.);
#2630=EDGE_CURVE('',#2214,#2215,#1438,.T.);
#2631=EDGE_CURVE('',#2215,#2215,#1899,.T.);
#2632=EDGE_CURVE('',#2216,#2216,#1900,.T.);
#2633=EDGE_CURVE('',#2216,#2217,#1439,.T.);
#2634=EDGE_CURVE('',#2217,#2217,#1901,.T.);
#3299=ORIENTED_EDGE('',*,*,#2629,.F.);
#3300=ORIENTED_EDGE('',*,*,#2630,.T.);
#3301=ORIENTED_EDGE('',*,*,#2631,.T.);
#3302=ORIENTED_EDGE('',*,*,#2630,.F.);
#3303=ORIENTED_EDGE('',*,*,#2632,.F.);
#3304=ORIENTED_EDGE('',*,*,#2633,.T.);
#3305=ORIENTED_EDGE('',*,*,#2634,.T.);
#3306=ORIENTED_EDGE('',*,*,#2633,.F.);
#3307=ORIENTED_EDGE('',*,*,#2632,.T.);
#3308=ORIENTED_EDGE('',*,*,#2629,.T.);
#3309=ORIENTED_EDGE('',*,*,#2634,.F.);
#3310=ORIENTED_EDGE('',*,*,#2631,.F.);
#4199=CYLINDRICAL_SURFACE('',#5052,0.32);
#4200=CYLINDRICAL_SURFACE('',#5055,0.6);
#4351=ADVANCED_FACE('',(#736),#4199,.F.);
#4352=ADVANCED_FACE('',(#737),#4200,.T.);
#4353=ADVANCED_FACE('',(#738,#428),#570,.T.);
#4354=ADVANCED_FACE('',(#739,#429),#571,.F.);
#4582=CLOSED_SHELL('',(#4351,#4352,#4353,#4354));
#5051=AXIS2_PLACEMENT_3D('',#8516,#5907,#5908);
#5052=AXIS2_PLACEMENT_3D('',#8517,#5909,#5910);
#5053=AXIS2_PLACEMENT_3D('',#8519,#5911,#5912);
#5054=AXIS2_PLACEMENT_3D('',#8522,#5914,#5915);
#5055=AXIS2_PLACEMENT_3D('',#8523,#5916,#5917);
#5056=AXIS2_PLACEMENT_3D('',#8525,#5918,#5919);
#5057=AXIS2_PLACEMENT_3D('',#8528,#5921,#5922);
#5058=AXIS2_PLACEMENT_3D('',#8529,#5923,#5924);
#5059=AXIS2_PLACEMENT_3D('',#8530,#5925,#5926);
#5907=DIRECTION('axis',(0.,0.,1.));
#5908=DIRECTION('refdir',(1.,0.,0.));
#5909=DIRECTION('center_axis',(0.,1.,0.));
#5910=DIRECTION('ref_axis',(1.,0.,0.));
#5911=DIRECTION('center_axis',(0.,-1.,0.));
#5912=DIRECTION('ref_axis',(1.,0.,0.));
#5913=DIRECTION('',(0.,-1.,0.));
#5914=DIRECTION('center_axis',(0.,-1.,0.));
#5915=DIRECTION('ref_axis',(1.,0.,0.));
#5916=DIRECTION('center_axis',(0.,1.,0.));
#5917=DIRECTION('ref_axis',(1.,0.,0.));
#5918=DIRECTION('center_axis',(0.,1.,0.));
#5919=DIRECTION('ref_axis',(1.,0.,0.));
#5920=DIRECTION('',(0.,-1.,0.));
#5921=DIRECTION('center_axis',(0.,1.,0.));
#5922=DIRECTION('ref_axis',(1.,0.,0.));
#5923=DIRECTION('center_axis',(0.,1.,0.));
#5924=DIRECTION('ref_axis',(1.,0.,0.));
#5925=DIRECTION('center_axis',(0.,1.,0.));
#5926=DIRECTION('ref_axis',(1.,0.,0.));
#8516=CARTESIAN_POINT('',(0.,0.,0.));
#8517=CARTESIAN_POINT('Origin',(0.,0.,0.));
#8518=CARTESIAN_POINT('',(-0.32,0.16,3.91886975727153E-17));
#8519=CARTESIAN_POINT('Origin',(0.,0.16,0.));
#8520=CARTESIAN_POINT('',(-0.32,0.,3.91886975727153E-17));
#8521=CARTESIAN_POINT('',(-0.32,0.,3.91886975727153E-17));
#8522=CARTESIAN_POINT('Origin',(0.,0.,0.));
#8523=CARTESIAN_POINT('Origin',(0.,0.,0.));
#8524=CARTESIAN_POINT('',(-0.6,0.16,7.34788079488412E-17));
#8525=CARTESIAN_POINT('Origin',(0.,0.16,0.));
#8526=CARTESIAN_POINT('',(-0.6,0.,7.34788079488412E-17));
#8527=CARTESIAN_POINT('',(-0.6,0.,7.34788079488412E-17));
#8528=CARTESIAN_POINT('Origin',(0.,0.,0.));
#8529=CARTESIAN_POINT('Origin',(0.,0.16,0.));
#8530=CARTESIAN_POINT('Origin',(0.,0.,0.));
#9968=UNCERTAINTY_MEASURE_WITH_UNIT(LENGTH_MEASURE(0.001),#10021,
'DISTANCE_ACCURACY_VALUE',
'Maximum model space distance between geometric entities at asserted c
onnectivities');
#9987=UNCERTAINTY_MEASURE_WITH_UNIT(LENGTH_MEASURE(0.001),#10021,
'DISTANCE_ACCURACY_VALUE',
'Maximum model space distance between geometric entities at asserted c
onnectivities');
#10001=(
GEOMETRIC_REPRESENTATION_CONTEXT(3)
GLOBAL_UNCERTAINTY_ASSIGNED_CONTEXT((#9968))
GLOBAL_UNIT_ASSIGNED_CONTEXT((#10021,#10023,#10024))
REPRESENTATION_CONTEXT('','3D')
);
#10020=(
GEOMETRIC_REPRESENTATION_CONTEXT(3)
GLOBAL_UNCERTAINTY_ASSIGNED_CONTEXT((#9987))
GLOBAL_UNIT_ASSIGNED_CONTEXT((#10021,#10023,#10024))
REPRESENTATION_CONTEXT('','3D')
);
#10021=(
LENGTH_UNIT()
NAMED_UNIT(*)
SI_UNIT(.CENTI.,.METRE.)
);
#10023=(
NAMED_UNIT(*)
PLANE_ANGLE_UNIT()
SI_UNIT($,.RADIAN.)
);
#10024=(
NAMED_UNIT(*)
SI_UNIT($,.STERADIAN.)
SOLID_ANGLE_UNIT()
);
#10038=SHAPE_DEFINITION_REPRESENTATION(#10070,#10148);
#10070=PRODUCT_DEFINITION_SHAPE('',$,#10181);
#10148=SHAPE_REPRESENTATION('',(#5051),#10001);
#10167=PRODUCT_DEFINITION_CONTEXT('part definition',#10265,'design');
#10181=PRODUCT_DEFINITION('Flat Washer - M6','Flat Washer - M6',#10213,
#10167);
#10213=PRODUCT_DEFINITION_FORMATION('',$,#10280);
#10265=APPLICATION_CONTEXT(
'Core Data for Automotive Mechanical Design Process');
#10266=PRODUCT_CONTEXT('part definition',#10265,'mechanical');
#10280=PRODUCT('Flat Washer - M6','Flat Washer - M6','Flat Washer - M6',
(#10266));
#10369=COLOUR_RGB('Black',0.12,0.14,0.17);
#10370=FILL_AREA_STYLE_COLOUR('',#10369);
#10371=FILL_AREA_STYLE('',(#10370));
#10372=SURFACE_STYLE_FILL_AREA(#10371);
#10373=SURFACE_SIDE_STYLE('',(#10372));
#10374=SURFACE_STYLE_USAGE(.BOTH.,#10373);
#10375=PRESENTATION_STYLE_ASSIGNMENT((#10374));
ENDSEC;
END-ISO-10303-21;
